ISO-10303-21;
HEADER;
/* Generated by software containing ST-Developer
 * from STEP Tools, Inc. (www.steptools.com) 
 */

FILE_DESCRIPTION(
/* description */ ('PAT-091'),
/* implementation_level */ '2;1');

FILE_NAME(
/* name */ 'M4 low-profile retaining screw (9).step',
/* time_stamp */ '2026-10-27T15:34:44-07:00',
/* author */ (''),
/* organization */ (''),
/* preprocessor_version */ 'ST-DEVELOPER v20.2',
/* originating_system */ 'Autodesk Translation Framework v15.17.0.0',
/* authorisation */ '');

FILE_SCHEMA (('AUTOMOTIVE_DESIGN { 1 0 10303 214 3 1 1 }'));
ENDSEC;

DATA;
#10=MECHANICAL_DESIGN_GEOMETRIC_PRESENTATION_REPRESENTATION('',(#1062),#25100);
#842=SHAPE_REPRESENTATION_RELATIONSHIP('SRR','None',#25609,#952);
#952=ADVANCED_BREP_SHAPE_REPRESENTATION('',(#1183),#25079);
#1062=STYLED_ITEM('',(#26198),#1183);
#1183=MANIFOLD_SOLID_BREP('Body1',#13342);
#1600=FACE_BOUND('',#3936,.T.);
#2001=PLANE('',#16042);
#2002=PLANE('',#16047);
#2003=PLANE('',#16050);
#2732=FACE_OUTER_BOUND('',#3935,.T.);
#2733=FACE_OUTER_BOUND('',#3937,.T.);
#2734=FACE_OUTER_BOUND('',#3938,.T.);
#2735=FACE_OUTER_BOUND('',#3939,.T.);
#2736=FACE_OUTER_BOUND('',#3940,.T.);
#3935=EDGE_LOOP('',(#11588));
#3936=EDGE_LOOP('',(#11589));
#3937=EDGE_LOOP('',(#11590,#11591,#11592,#11593));
#3938=EDGE_LOOP('',(#11594));
#3939=EDGE_LOOP('',(#11595,#11596,#11597,#11598));
#3940=EDGE_LOOP('',(#11599));
#4814=LINE('',#24052,#5554);
#4815=LINE('',#24058,#5555);
#5554=VECTOR('',#20080,0.350000000000001);
#5555=VECTOR('',#20089,0.199999999999999);
#6218=CIRCLE('',#16043,0.350000000000001);
#6219=CIRCLE('',#16044,0.199999999999999);
#6220=CIRCLE('',#16046,0.350000000000001);
#6221=CIRCLE('',#16049,0.199999999999999);
#7251=VERTEX_POINT('',#24046);
#7252=VERTEX_POINT('',#24048);
#7253=VERTEX_POINT('',#24051);
#7254=VERTEX_POINT('',#24056);
#8729=EDGE_CURVE('',#7251,#7251,#6218,.T.);
#8730=EDGE_CURVE('',#7252,#7252,#6219,.T.);
#8731=EDGE_CURVE('',#7251,#7253,#4814,.T.);
#8732=EDGE_CURVE('',#7253,#7253,#6220,.T.);
#8733=EDGE_CURVE('',#7254,#7254,#6221,.T.);
#8734=EDGE_CURVE('',#7254,#7252,#4815,.T.);
#11588=ORIENTED_EDGE('',*,*,#8729,.T.);
#11589=ORIENTED_EDGE('',*,*,#8730,.F.);
#11590=ORIENTED_EDGE('',*,*,#8729,.F.);
#11591=ORIENTED_EDGE('',*,*,#8731,.T.);
#11592=ORIENTED_EDGE('',*,*,#8732,.T.);
#11593=ORIENTED_EDGE('',*,*,#8731,.F.);
#11594=ORIENTED_EDGE('',*,*,#8732,.F.);
#11595=ORIENTED_EDGE('',*,*,#8733,.F.);
#11596=ORIENTED_EDGE('',*,*,#8734,.T.);
#11597=ORIENTED_EDGE('',*,*,#8730,.T.);
#11598=ORIENTED_EDGE('',*,*,#8734,.F.);
#11599=ORIENTED_EDGE('',*,*,#8733,.T.);
#12370=CYLINDRICAL_SURFACE('',#16045,0.350000000000001);
#12371=CYLINDRICAL_SURFACE('',#16048,0.199999999999999);
#13099=ADVANCED_FACE('',(#2732,#1600),#2001,.T.);
#13100=ADVANCED_FACE('',(#2733),#12370,.T.);
#13101=ADVANCED_FACE('',(#2734),#2002,.F.);
#13102=ADVANCED_FACE('',(#2735),#12371,.T.);
#13103=ADVANCED_FACE('',(#2736),#2003,.T.);
#13342=CLOSED_SHELL('',(#13099,#13100,#13101,#13102,#13103));
#16041=AXIS2_PLACEMENT_3D('',#24044,#20070,#20071);
#16042=AXIS2_PLACEMENT_3D('',#24045,#20072,#20073);
#16043=AXIS2_PLACEMENT_3D('',#24047,#20074,#20075);
#16044=AXIS2_PLACEMENT_3D('',#24049,#20076,#20077);
#16045=AXIS2_PLACEMENT_3D('',#24050,#20078,#20079);
#16046=AXIS2_PLACEMENT_3D('',#24053,#20081,#20082);
#16047=AXIS2_PLACEMENT_3D('',#24054,#20083,#20084);
#16048=AXIS2_PLACEMENT_3D('',#24055,#20085,#20086);
#16049=AXIS2_PLACEMENT_3D('',#24057,#20087,#20088);
#16050=AXIS2_PLACEMENT_3D('',#24059,#20090,#20091);
#20070=DIRECTION('axis',(0.,0.,1.));
#20071=DIRECTION('refdir',(1.,0.,0.));
#20072=DIRECTION('center_axis',(0.,1.,0.));
#20073=DIRECTION('ref_axis',(1.,0.,0.));
#20074=DIRECTION('center_axis',(0.,1.,0.));
#20075=DIRECTION('ref_axis',(1.,0.,0.));
#20076=DIRECTION('center_axis',(0.,1.,0.));
#20077=DIRECTION('ref_axis',(1.,0.,0.));
#20078=DIRECTION('center_axis',(0.,1.,0.));
#20079=DIRECTION('ref_axis',(1.,0.,0.));
#20080=DIRECTION('',(0.,-1.,0.));
#20081=DIRECTION('center_axis',(0.,1.,0.));
#20082=DIRECTION('ref_axis',(1.,0.,0.));
#20083=DIRECTION('center_axis',(0.,1.,0.));
#20084=DIRECTION('ref_axis',(1.,0.,0.));
#20085=DIRECTION('center_axis',(0.,1.,0.));
#20086=DIRECTION('ref_axis',(1.,0.,0.));
#20087=DIRECTION('center_axis',(0.,1.,0.));
#20088=DIRECTION('ref_axis',(1.,0.,0.));
#20089=DIRECTION('',(0.,-1.,0.));
#20090=DIRECTION('center_axis',(0.,1.,0.));
#20091=DIRECTION('ref_axis',(1.,0.,0.));
#24044=CARTESIAN_POINT('',(0.,0.,0.));
#24045=CARTESIAN_POINT('Origin',(18.056769185842,6.7,9.30814754519511));
#24046=CARTESIAN_POINT('',(17.706769185842,6.7,9.30814754519511));
#24047=CARTESIAN_POINT('Origin',(18.056769185842,6.7,9.30814754519511));
#24048=CARTESIAN_POINT('',(17.856769185842,6.7,9.30814754519511));
#24049=CARTESIAN_POINT('Origin',(18.056769185842,6.7,9.30814754519511));
#24050=CARTESIAN_POINT('Origin',(18.056769185842,6.6,9.30814754519511));
#24051=CARTESIAN_POINT('',(17.706769185842,6.6,9.30814754519511));
#24052=CARTESIAN_POINT('',(17.706769185842,6.6,9.30814754519511));
#24053=CARTESIAN_POINT('Origin',(18.056769185842,6.6,9.30814754519511));
#24054=CARTESIAN_POINT('Origin',(18.056769185842,6.6,9.30814754519511));
#24055=CARTESIAN_POINT('Origin',(18.056769185842,6.7,9.30814754519511));
#24056=CARTESIAN_POINT('',(17.856769185842,7.4,9.30814754519511));
#24057=CARTESIAN_POINT('Origin',(18.056769185842,7.4,9.30814754519511));
#24058=CARTESIAN_POINT('',(17.856769185842,6.7,9.30814754519511));
#24059=CARTESIAN_POINT('Origin',(18.056769185842,7.4,9.30814754519511));
#24958=UNCERTAINTY_MEASURE_WITH_UNIT(LENGTH_MEASURE(0.001),#25101,
'DISTANCE_ACCURACY_VALUE',
'Maximum model space distance between geometric entities at asserted c
onnectivities');
#24979=UNCERTAINTY_MEASURE_WITH_UNIT(LENGTH_MEASURE(0.001),#25101,
'DISTANCE_ACCURACY_VALUE',
'Maximum model space distance between geometric entities at asserted c
onnectivities');
#25079=(
GEOMETRIC_REPRESENTATION_CONTEXT(3)
GLOBAL_UNCERTAINTY_ASSIGNED_CONTEXT((#24958))
GLOBAL_UNIT_ASSIGNED_CONTEXT((#25101,#25103,#25104))
REPRESENTATION_CONTEXT('','3D')
);
#25100=(
GEOMETRIC_REPRESENTATION_CONTEXT(3)
GLOBAL_UNCERTAINTY_ASSIGNED_CONTEXT((#24979))
GLOBAL_UNIT_ASSIGNED_CONTEXT((#25101,#25103,#25104))
REPRESENTATION_CONTEXT('','3D')
);
#25101=(
LENGTH_UNIT()
NAMED_UNIT(*)
SI_UNIT(.CENTI.,.METRE.)
);
#25103=(
NAMED_UNIT(*)
PLANE_ANGLE_UNIT()
SI_UNIT($,.RADIAN.)
);
#25104=(
NAMED_UNIT(*)
SI_UNIT($,.STERADIAN.)
SOLID_ANGLE_UNIT()
);
#25204=SHAPE_DEFINITION_REPRESENTATION(#25398,#25609);
#25398=PRODUCT_DEFINITION_SHAPE('',$,#25730);
#25609=SHAPE_REPRESENTATION('',(#16041),#25079);
#25630=PRODUCT_DEFINITION_CONTEXT('part definition',#25992,'design');
#25730=PRODUCT_DEFINITION('M4 low-profile retaining screw (9)',
'M4 low-profile retaining screw (9)',#25850,#25630);
#25850=PRODUCT_DEFINITION_FORMATION('',$,#26093);
#25992=APPLICATION_CONTEXT(
'Core Data for Automotive Mechanical Design Process');
#25993=PRODUCT_CONTEXT('part definition',#25992,'mechanical');
#26093=PRODUCT('M4 low-profile retaining screw (9)',
'M4 low-profile retaining screw (9)','M4 low-profile retaining screw (9)',(#25993));
#26192=COLOUR_RGB('Black',0.12,0.14,0.17);
#26193=FILL_AREA_STYLE_COLOUR('',#26192);
#26194=FILL_AREA_STYLE('',(#26193));
#26195=SURFACE_STYLE_FILL_AREA(#26194);
#26196=SURFACE_SIDE_STYLE('',(#26195));
#26197=SURFACE_STYLE_USAGE(.BOTH.,#26196);
#26198=PRESENTATION_STYLE_ASSIGNMENT((#26197));
ENDSEC;
END-ISO-10303-21;
